ISO-10303-21;
HEADER;
/* Generated by software containing ST-Developer
 * from STEP Tools, Inc. (www.steptools.com) 
 */

FILE_DESCRIPTION(
/* description */ ('Bearing friction torque test rig'),
/* implementation_level */ '2;1');

FILE_NAME(
/* name */ 'Balls (1).step',
/* time_stamp */ '2026-10-28T03:24:04-07:00',
/* author */ (''),
/* organization */ (''),
/* preprocessor_version */ 'ST-DEVELOPER v20.2',
/* originating_system */ 'Autodesk Translation Framework v15.17.0.0',
/* authorisation */ '');

FILE_SCHEMA (('AUTOMOTIVE_DESIGN { 1 0 10303 214 3 1 1 }'));
ENDSEC;

DATA;
#10=MECHANICAL_DESIGN_GEOMETRIC_PRESENTATION_REPRESENTATION('',(#569,#570,#571,#572,#573,#574,#575,#576),#14822);
#409=SPHERICAL_SURFACE('',#8792,0.3969);
#410=SPHERICAL_SURFACE('',#8794,0.3969);
#411=SPHERICAL_SURFACE('',#8796,0.3969);
#412=SPHERICAL_SURFACE('',#8798,0.3969);
#413=SPHERICAL_SURFACE('',#8800,0.3969);
#414=SPHERICAL_SURFACE('',#8802,0.3969);
#415=SPHERICAL_SURFACE('',#8804,0.3969);
#416=SPHERICAL_SURFACE('',#8806,0.3969);
#484=SHAPE_REPRESENTATION_RELATIONSHIP('SRR','None',#15025,#523);
#523=ADVANCED_BREP_SHAPE_REPRESENTATION('',(#622,#623,#624,#625,#626,#627,
#628,#629),#14805);
#569=STYLED_ITEM('',(#15284),#622);
#570=STYLED_ITEM('',(#15284),#623);
#571=STYLED_ITEM('',(#15284),#624);
#572=STYLED_ITEM('',(#15284),#625);
#573=STYLED_ITEM('',(#15284),#626);
#574=STYLED_ITEM('',(#15284),#627);
#575=STYLED_ITEM('',(#15284),#628);
#576=STYLED_ITEM('',(#15284),#629);
#622=MANIFOLD_SOLID_BREP('Body1',#7686);
#623=MANIFOLD_SOLID_BREP('Body2',#7687);
#624=MANIFOLD_SOLID_BREP('Body3',#7688);
#625=MANIFOLD_SOLID_BREP('Body4',#7689);
#626=MANIFOLD_SOLID_BREP('Body5',#7690);
#627=MANIFOLD_SOLID_BREP('Body6',#7691);
#628=MANIFOLD_SOLID_BREP('Body7',#7692);
#629=MANIFOLD_SOLID_BREP('Body8',#7693);
#1400=FACE_OUTER_BOUND('',#2028,.T.);
#1401=FACE_OUTER_BOUND('',#2029,.T.);
#1402=FACE_OUTER_BOUND('',#2030,.T.);
#1403=FACE_OUTER_BOUND('',#2031,.T.);
#1404=FACE_OUTER_BOUND('',#2032,.T.);
#1405=FACE_OUTER_BOUND('',#2033,.T.);
#1406=FACE_OUTER_BOUND('',#2034,.T.);
#1407=FACE_OUTER_BOUND('',#2035,.T.);
#2028=EDGE_LOOP('',(#6466,#6467));
#2029=EDGE_LOOP('',(#6468,#6469));
#2030=EDGE_LOOP('',(#6470,#6471));
#2031=EDGE_LOOP('',(#6472,#6473));
#2032=EDGE_LOOP('',(#6474,#6475));
#2033=EDGE_LOOP('',(#6476,#6477));
#2034=EDGE_LOOP('',(#6478,#6479));
#2035=EDGE_LOOP('',(#6480,#6481));
#3417=CIRCLE('',#8793,0.3969);
#3418=CIRCLE('',#8795,0.3969);
#3419=CIRCLE('',#8797,0.3969);
#3420=CIRCLE('',#8799,0.3969);
#3421=CIRCLE('',#8801,0.3969);
#3422=CIRCLE('',#8803,0.3969);
#3423=CIRCLE('',#8805,0.3969);
#3424=CIRCLE('',#8807,0.3969);
#3998=VERTEX_POINT('',#13391);
#3999=VERTEX_POINT('',#13392);
#4000=VERTEX_POINT('',#13395);
#4001=VERTEX_POINT('',#13396);
#4002=VERTEX_POINT('',#13399);
#4003=VERTEX_POINT('',#13400);
#4004=VERTEX_POINT('',#13403);
#4005=VERTEX_POINT('',#13404);
#4006=VERTEX_POINT('',#13407);
#4007=VERTEX_POINT('',#13408);
#4008=VERTEX_POINT('',#13411);
#4009=VERTEX_POINT('',#13412);
#4010=VERTEX_POINT('',#13415);
#4011=VERTEX_POINT('',#13416);
#4012=VERTEX_POINT('',#13419);
#4013=VERTEX_POINT('',#13420);
#4859=EDGE_CURVE('',#3998,#3999,#3417,.T.);
#4860=EDGE_CURVE('',#4000,#4001,#3418,.T.);
#4861=EDGE_CURVE('',#4002,#4003,#3419,.T.);
#4862=EDGE_CURVE('',#4004,#4005,#3420,.T.);
#4863=EDGE_CURVE('',#4006,#4007,#3421,.T.);
#4864=EDGE_CURVE('',#4008,#4009,#3422,.T.);
#4865=EDGE_CURVE('',#4010,#4011,#3423,.T.);
#4866=EDGE_CURVE('',#4012,#4013,#3424,.T.);
#6466=ORIENTED_EDGE('',*,*,#4859,.T.);
#6467=ORIENTED_EDGE('',*,*,#4859,.F.);
#6468=ORIENTED_EDGE('',*,*,#4860,.T.);
#6469=ORIENTED_EDGE('',*,*,#4860,.F.);
#6470=ORIENTED_EDGE('',*,*,#4861,.T.);
#6471=ORIENTED_EDGE('',*,*,#4861,.F.);
#6472=ORIENTED_EDGE('',*,*,#4862,.T.);
#6473=ORIENTED_EDGE('',*,*,#4862,.F.);
#6474=ORIENTED_EDGE('',*,*,#4863,.T.);
#6475=ORIENTED_EDGE('',*,*,#4863,.F.);
#6476=ORIENTED_EDGE('',*,*,#4864,.T.);
#6477=ORIENTED_EDGE('',*,*,#4864,.F.);
#6478=ORIENTED_EDGE('',*,*,#4865,.T.);
#6479=ORIENTED_EDGE('',*,*,#4865,.F.);
#6480=ORIENTED_EDGE('',*,*,#4866,.T.);
#6481=ORIENTED_EDGE('',*,*,#4866,.F.);
#7511=ADVANCED_FACE('',(#1400),#409,.T.);
#7512=ADVANCED_FACE('',(#1401),#410,.T.);
#7513=ADVANCED_FACE('',(#1402),#411,.T.);
#7514=ADVANCED_FACE('',(#1403),#412,.T.);
#7515=ADVANCED_FACE('',(#1404),#413,.T.);
#7516=ADVANCED_FACE('',(#1405),#414,.T.);
#7517=ADVANCED_FACE('',(#1406),#415,.T.);
#7518=ADVANCED_FACE('',(#1407),#416,.T.);
#7686=CLOSED_SHELL('',(#7511));
#7687=CLOSED_SHELL('',(#7512));
#7688=CLOSED_SHELL('',(#7513));
#7689=CLOSED_SHELL('',(#7514));
#7690=CLOSED_SHELL('',(#7515));
#7691=CLOSED_SHELL('',(#7516));
#7692=CLOSED_SHELL('',(#7517));
#7693=CLOSED_SHELL('',(#7518));
#8791=AXIS2_PLACEMENT_3D('',#13389,#10793,#10794);
#8792=AXIS2_PLACEMENT_3D('',#13390,#10795,#10796);
#8793=AXIS2_PLACEMENT_3D('',#13393,#10797,#10798);
#8794=AXIS2_PLACEMENT_3D('',#13394,#10799,#10800);
#8795=AXIS2_PLACEMENT_3D('',#13397,#10801,#10802);
#8796=AXIS2_PLACEMENT_3D('',#13398,#10803,#10804);
#8797=AXIS2_PLACEMENT_3D('',#13401,#10805,#10806);
#8798=AXIS2_PLACEMENT_3D('',#13402,#10807,#10808);
#8799=AXIS2_PLACEMENT_3D('',#13405,#10809,#10810);
#8800=AXIS2_PLACEMENT_3D('',#13406,#10811,#10812);
#8801=AXIS2_PLACEMENT_3D('',#13409,#10813,#10814);
#8802=AXIS2_PLACEMENT_3D('',#13410,#10815,#10816);
#8803=AXIS2_PLACEMENT_3D('',#13413,#10817,#10818);
#8804=AXIS2_PLACEMENT_3D('',#13414,#10819,#10820);
#8805=AXIS2_PLACEMENT_3D('',#13417,#10821,#10822);
#8806=AXIS2_PLACEMENT_3D('',#13418,#10823,#10824);
#8807=AXIS2_PLACEMENT_3D('',#13421,#10825,#10826);
#10793=DIRECTION('axis',(0.,0.,1.));
#10794=DIRECTION('refdir',(1.,0.,0.));
#10795=DIRECTION('center_axis',(0.,0.,1.));
#10796=DIRECTION('ref_axis',(1.,0.,0.));
#10797=DIRECTION('center_axis',(1.22464679914735E-16,-1.,0.));
#10798=DIRECTION('ref_axis',(-1.,-1.22464679914735E-16,0.));
#10799=DIRECTION('center_axis',(0.707106781186548,0.,0.707106781186548));
#10800=DIRECTION('ref_axis',(0.707106781186548,0.,-0.707106781186548));
#10801=DIRECTION('center_axis',(8.65956056235493E-17,-1.,-8.65956056235493E-17));
#10802=DIRECTION('ref_axis',(-0.707106781186548,-1.22464679914735E-16,0.707106781186548));
#10803=DIRECTION('center_axis',(1.,0.,0.));
#10804=DIRECTION('ref_axis',(6.12323399573677E-17,0.,-1.));
#10805=DIRECTION('center_axis',(7.49879891330929E-33,-1.,-1.22464679914735E-16));
#10806=DIRECTION('ref_axis',(-6.12323399573677E-17,-1.22464679914735E-16,
1.));
#10807=DIRECTION('center_axis',(0.707106781186548,0.,-0.707106781186548));
#10808=DIRECTION('ref_axis',(-0.707106781186548,0.,-0.707106781186548));
#10809=DIRECTION('center_axis',(-8.65956056235493E-17,-1.,-8.65956056235493E-17));
#10810=DIRECTION('ref_axis',(0.707106781186548,-1.22464679914735E-16,0.707106781186548));
#10811=DIRECTION('center_axis',(0.,0.,-1.));
#10812=DIRECTION('ref_axis',(-1.,0.,-1.22464679914735E-16));
#10813=DIRECTION('center_axis',(-1.22464679914735E-16,-1.,-1.49975978266186E-32));
#10814=DIRECTION('ref_axis',(1.,-1.22464679914735E-16,1.22464679914735E-16));
#10815=DIRECTION('center_axis',(-0.707106781186548,0.,-0.707106781186548));
#10816=DIRECTION('ref_axis',(-0.707106781186548,0.,0.707106781186548));
#10817=DIRECTION('center_axis',(-8.65956056235493E-17,-1.,8.65956056235493E-17));
#10818=DIRECTION('ref_axis',(0.707106781186548,-1.22464679914735E-16,-0.707106781186548));
#10819=DIRECTION('center_axis',(-1.,0.,0.));
#10820=DIRECTION('ref_axis',(-1.83697019872103E-16,0.,1.));
#10821=DIRECTION('center_axis',(-2.24963967399279E-32,-1.,1.22464679914735E-16));
#10822=DIRECTION('ref_axis',(1.83697019872103E-16,-1.22464679914735E-16,
-1.));
#10823=DIRECTION('center_axis',(-0.707106781186548,0.,0.707106781186548));
#10824=DIRECTION('ref_axis',(0.707106781186548,0.,0.707106781186548));
#10825=DIRECTION('center_axis',(8.65956056235493E-17,-1.,8.65956056235494E-17));
#10826=DIRECTION('ref_axis',(-0.707106781186548,-1.22464679914735E-16,-0.707106781186548));
#13389=CARTESIAN_POINT('',(0.,0.,0.));
#13390=CARTESIAN_POINT('Origin',(1.675,0.,0.));
#13391=CARTESIAN_POINT('',(1.675,-2.97627328869245E-33,0.3969));
#13392=CARTESIAN_POINT('',(1.675,-2.97627328869245E-33,-0.3969));
#13393=CARTESIAN_POINT('Origin',(1.675,0.,0.));
#13394=CARTESIAN_POINT('Origin',(1.18440385848747,0.,-1.18440385848747));
#13395=CARTESIAN_POINT('',(1.46505453994041,3.1867025333467E-33,-0.903753177034526));
#13396=CARTESIAN_POINT('',(0.903753177034527,-9.13924911073161E-33,-1.46505453994041));
#13397=CARTESIAN_POINT('Origin',(1.18440385848747,0.,-1.18440385848747));
#13398=CARTESIAN_POINT('Origin',(1.02564169428591E-16,0.,-1.675));
#13399=CARTESIAN_POINT('',(0.3969,-2.97627328869246E-33,-1.675));
#13400=CARTESIAN_POINT('',(-0.3969,-2.97627328869245E-33,-1.675));
#13401=CARTESIAN_POINT('Origin',(1.02564169428591E-16,0.,-1.675));
#13402=CARTESIAN_POINT('Origin',(-1.18440385848747,0.,-1.18440385848747));
#13403=CARTESIAN_POINT('',(-0.903753177034526,3.1867025333467E-33,-1.46505453994041));
#13404=CARTESIAN_POINT('',(-1.46505453994041,-9.13924911073161E-33,-0.903753177034527));
#13405=CARTESIAN_POINT('Origin',(-1.18440385848747,0.,-1.18440385848747));
#13406=CARTESIAN_POINT('Origin',(-1.675,0.,-2.05128338857182E-16));
#13407=CARTESIAN_POINT('',(-1.675,-2.97627328869246E-33,-0.3969));
#13408=CARTESIAN_POINT('',(-1.675,-2.97627328869245E-33,0.3969));
#13409=CARTESIAN_POINT('Origin',(-1.675,0.,-2.05128338857182E-16));
#13410=CARTESIAN_POINT('Origin',(-1.18440385848747,0.,1.18440385848747));
#13411=CARTESIAN_POINT('',(-1.46505453994041,6.26819044436628E-33,0.903753177034526));
#13412=CARTESIAN_POINT('',(-0.903753177034527,-1.22207370217512E-32,1.46505453994041));
#13413=CARTESIAN_POINT('Origin',(-1.18440385848747,0.,1.18440385848747));
#13414=CARTESIAN_POINT('Origin',(-3.07692508285772E-16,0.,1.675));
#13415=CARTESIAN_POINT('',(-0.3969,-2.97627328869246E-33,1.675));
#13416=CARTESIAN_POINT('',(0.396899999999999,-2.97627328869245E-33,1.675));
#13417=CARTESIAN_POINT('Origin',(-3.07692508285772E-16,0.,1.675));
#13418=CARTESIAN_POINT('Origin',(1.18440385848747,0.,1.18440385848747));
#13419=CARTESIAN_POINT('',(0.903753177034526,9.34967835538585E-33,1.46505453994041));
#13420=CARTESIAN_POINT('',(1.46505453994041,-1.53022249327708E-32,0.903753177034527));
#13421=CARTESIAN_POINT('Origin',(1.18440385848747,0.,1.18440385848747));
#14760=UNCERTAINTY_MEASURE_WITH_UNIT(LENGTH_MEASURE(0.001),#14823,
'DISTANCE_ACCURACY_VALUE',
'Maximum model space distance between geometric entities at asserted c
onnectivities');
#14777=UNCERTAINTY_MEASURE_WITH_UNIT(LENGTH_MEASURE(0.001),#14823,
'DISTANCE_ACCURACY_VALUE',
'Maximum model space distance between geometric entities at asserted c
onnectivities');
#14805=(
GEOMETRIC_REPRESENTATION_CONTEXT(3)
GLOBAL_UNCERTAINTY_ASSIGNED_CONTEXT((#14760))
GLOBAL_UNIT_ASSIGNED_CONTEXT((#14823,#14825,#14826))
REPRESENTATION_CONTEXT('','3D')
);
#14822=(
GEOMETRIC_REPRESENTATION_CONTEXT(3)
GLOBAL_UNCERTAINTY_ASSIGNED_CONTEXT((#14777))
GLOBAL_UNIT_ASSIGNED_CONTEXT((#14823,#14825,#14826))
REPRESENTATION_CONTEXT('','3D')
);
#14823=(
LENGTH_UNIT()
NAMED_UNIT(*)
SI_UNIT(.CENTI.,.METRE.)
);
#14825=(
NAMED_UNIT(*)
PLANE_ANGLE_UNIT()
SI_UNIT($,.RADIAN.)
);
#14826=(
NAMED_UNIT(*)
SI_UNIT($,.STERADIAN.)
SOLID_ANGLE_UNIT()
);
#14854=SHAPE_DEFINITION_REPRESENTATION(#14903,#15025);
#14903=PRODUCT_DEFINITION_SHAPE('',$,#15070);
#15025=SHAPE_REPRESENTATION('',(#8791),#14805);
#15042=PRODUCT_DEFINITION_CONTEXT('part definition',#15176,'design');
#15070=PRODUCT_DEFINITION('Balls (1)','Balls (1)',#15114,#15042);
#15114=PRODUCT_DEFINITION_FORMATION('',$,#15205);
#15176=APPLICATION_CONTEXT(
'Core Data for Automotive Mechanical Design Process');
#15177=PRODUCT_CONTEXT('part definition',#15176,'mechanical');
#15205=PRODUCT('Balls (1)','Balls (1)','Balls (1)',(#15177));
#15278=COLOUR_RGB('Grey',0.48,0.52,0.57);
#15279=FILL_AREA_STYLE_COLOUR('',#15278);
#15280=FILL_AREA_STYLE('',(#15279));
#15281=SURFACE_STYLE_FILL_AREA(#15280);
#15282=SURFACE_SIDE_STYLE('',(#15281));
#15283=SURFACE_STYLE_USAGE(.BOTH.,#15282);
#15284=PRESENTATION_STYLE_ASSIGNMENT((#15283));
ENDSEC;
END-ISO-10303-21;
